ISO-10303-21;
HEADER;
/* Generated by software containing ST-Developer
 * from STEP Tools, Inc. (www.steptools.com) 
 */

FILE_DESCRIPTION(
/* description */ ('Torque wrench calibration arm'),
/* implementation_level */ '2;1');

FILE_NAME(
/* name */ 'Bearing cap (1).step',
/* time_stamp */ '2026-10-28T03:24:52-07:00',
/* author */ (''),
/* organization */ (''),
/* preprocessor_version */ 'ST-DEVELOPER v20.2',
/* originating_system */ 'Autodesk Translation Framework v15.17.0.0',
/* authorisation */ '');

FILE_SCHEMA (('AUTOMOTIVE_DESIGN { 1 0 10303 214 3 1 1 }'));
ENDSEC;

DATA;
#10=MECHANICAL_DESIGN_GEOMETRIC_PRESENTATION_REPRESENTATION('',(#430),#12783);
#356=SHAPE_REPRESENTATION_RELATIONSHIP('SRR','None',#12937,#393);
#393=ADVANCED_BREP_SHAPE_REPRESENTATION('',(#484),#12746);
#430=STYLED_ITEM('',(#13212),#484);
#484=MANIFOLD_SOLID_BREP('Body1',#6499);
#572=FACE_BOUND('',#1395,.T.);
#573=FACE_BOUND('',#1399,.T.);
#574=FACE_BOUND('',#1400,.T.);
#575=FACE_BOUND('',#1401,.T.);
#576=FACE_BOUND('',#1402,.T.);
#577=FACE_BOUND('',#1403,.T.);
#578=FACE_BOUND('',#1405,.T.);
#579=FACE_BOUND('',#1406,.T.);
#580=FACE_BOUND('',#1407,.T.);
#581=FACE_BOUND('',#1408,.T.);
#582=FACE_BOUND('',#1409,.T.);
#695=PLANE('',#7134);
#696=PLANE('',#7141);
#697=PLANE('',#7142);
#953=FACE_OUTER_BOUND('',#1389,.T.);
#954=FACE_OUTER_BOUND('',#1390,.T.);
#955=FACE_OUTER_BOUND('',#1391,.T.);
#956=FACE_OUTER_BOUND('',#1392,.T.);
#957=FACE_OUTER_BOUND('',#1393,.T.);
#958=FACE_OUTER_BOUND('',#1394,.T.);
#959=FACE_OUTER_BOUND('',#1396,.T.);
#960=FACE_OUTER_BOUND('',#1397,.T.);
#961=FACE_OUTER_BOUND('',#1398,.T.);
#962=FACE_OUTER_BOUND('',#1404,.T.);
#1389=EDGE_LOOP('',(#4705,#4706,#4707,#4708));
#1390=EDGE_LOOP('',(#4709,#4710,#4711,#4712));
#1391=EDGE_LOOP('',(#4713,#4714,#4715,#4716));
#1392=EDGE_LOOP('',(#4717,#4718,#4719,#4720));
#1393=EDGE_LOOP('',(#4721,#4722,#4723,#4724));
#1394=EDGE_LOOP('',(#4725));
#1395=EDGE_LOOP('',(#4726));
#1396=EDGE_LOOP('',(#4727,#4728,#4729,#4730));
#1397=EDGE_LOOP('',(#4731,#4732,#4733,#4734));
#1398=EDGE_LOOP('',(#4735));
#1399=EDGE_LOOP('',(#4736));
#1400=EDGE_LOOP('',(#4737));
#1401=EDGE_LOOP('',(#4738));
#1402=EDGE_LOOP('',(#4739));
#1403=EDGE_LOOP('',(#4740));
#1404=EDGE_LOOP('',(#4741));
#1405=EDGE_LOOP('',(#4742));
#1406=EDGE_LOOP('',(#4743));
#1407=EDGE_LOOP('',(#4744));
#1408=EDGE_LOOP('',(#4745));
#1409=EDGE_LOOP('',(#4746));
#1889=LINE('',#10309,#2304);
#1890=LINE('',#10315,#2305);
#1891=LINE('',#10321,#2306);
#1892=LINE('',#10327,#2307);
#1893=LINE('',#10333,#2308);
#1894=LINE('',#10341,#2309);
#1895=LINE('',#10346,#2310);
#2304=VECTOR('',#8235,0.225);
#2305=VECTOR('',#8242,0.225);
#2306=VECTOR('',#8249,0.225);
#2307=VECTOR('',#8256,0.225);
#2308=VECTOR('',#8263,2.59);
#2309=VECTOR('',#8274,2.);
#2310=VECTOR('',#8279,4.);
#2690=CIRCLE('',#7120,0.225);
#2691=CIRCLE('',#7121,0.225);
#2692=CIRCLE('',#7123,0.225);
#2693=CIRCLE('',#7124,0.225);
#2694=CIRCLE('',#7126,0.225);
#2695=CIRCLE('',#7127,0.225);
#2696=CIRCLE('',#7129,0.225);
#2697=CIRCLE('',#7130,0.225);
#2698=CIRCLE('',#7132,2.59);
#2699=CIRCLE('',#7133,2.59);
#2700=CIRCLE('',#7135,2.);
#2701=CIRCLE('',#7137,2.);
#2702=CIRCLE('',#7139,4.);
#2703=CIRCLE('',#7140,4.);
#3089=VERTEX_POINT('',#10306);
#3090=VERTEX_POINT('',#10308);
#3091=VERTEX_POINT('',#10312);
#3092=VERTEX_POINT('',#10314);
#3093=VERTEX_POINT('',#10318);
#3094=VERTEX_POINT('',#10320);
#3095=VERTEX_POINT('',#10324);
#3096=VERTEX_POINT('',#10326);
#3097=VERTEX_POINT('',#10330);
#3098=VERTEX_POINT('',#10332);
#3099=VERTEX_POINT('',#10336);
#3100=VERTEX_POINT('',#10339);
#3101=VERTEX_POINT('',#10343);
#3102=VERTEX_POINT('',#10345);
#3710=EDGE_CURVE('',#3089,#3089,#2690,.T.);
#3711=EDGE_CURVE('',#3089,#3090,#1889,.T.);
#3712=EDGE_CURVE('',#3090,#3090,#2691,.T.);
#3713=EDGE_CURVE('',#3091,#3091,#2692,.T.);
#3714=EDGE_CURVE('',#3091,#3092,#1890,.T.);
#3715=EDGE_CURVE('',#3092,#3092,#2693,.T.);
#3716=EDGE_CURVE('',#3093,#3093,#2694,.T.);
#3717=EDGE_CURVE('',#3093,#3094,#1891,.T.);
#3718=EDGE_CURVE('',#3094,#3094,#2695,.T.);
#3719=EDGE_CURVE('',#3095,#3095,#2696,.T.);
#3720=EDGE_CURVE('',#3095,#3096,#1892,.T.);
#3721=EDGE_CURVE('',#3096,#3096,#2697,.T.);
#3722=EDGE_CURVE('',#3097,#3097,#2698,.T.);
#3723=EDGE_CURVE('',#3097,#3098,#1893,.T.);
#3724=EDGE_CURVE('',#3098,#3098,#2699,.T.);
#3725=EDGE_CURVE('',#3099,#3099,#2700,.T.);
#3726=EDGE_CURVE('',#3100,#3100,#2701,.T.);
#3727=EDGE_CURVE('',#3100,#3099,#1894,.T.);
#3728=EDGE_CURVE('',#3101,#3101,#2702,.T.);
#3729=EDGE_CURVE('',#3101,#3102,#1895,.T.);
#3730=EDGE_CURVE('',#3102,#3102,#2703,.T.);
#4705=ORIENTED_EDGE('',*,*,#3710,.F.);
#4706=ORIENTED_EDGE('',*,*,#3711,.T.);
#4707=ORIENTED_EDGE('',*,*,#3712,.F.);
#4708=ORIENTED_EDGE('',*,*,#3711,.F.);
#4709=ORIENTED_EDGE('',*,*,#3713,.F.);
#4710=ORIENTED_EDGE('',*,*,#3714,.T.);
#4711=ORIENTED_EDGE('',*,*,#3715,.F.);
#4712=ORIENTED_EDGE('',*,*,#3714,.F.);
#4713=ORIENTED_EDGE('',*,*,#3716,.F.);
#4714=ORIENTED_EDGE('',*,*,#3717,.T.);
#4715=ORIENTED_EDGE('',*,*,#3718,.F.);
#4716=ORIENTED_EDGE('',*,*,#3717,.F.);
#4717=ORIENTED_EDGE('',*,*,#3719,.F.);
#4718=ORIENTED_EDGE('',*,*,#3720,.T.);
#4719=ORIENTED_EDGE('',*,*,#3721,.F.);
#4720=ORIENTED_EDGE('',*,*,#3720,.F.);
#4721=ORIENTED_EDGE('',*,*,#3722,.F.);
#4722=ORIENTED_EDGE('',*,*,#3723,.T.);
#4723=ORIENTED_EDGE('',*,*,#3724,.T.);
#4724=ORIENTED_EDGE('',*,*,#3723,.F.);
#4725=ORIENTED_EDGE('',*,*,#3724,.F.);
#4726=ORIENTED_EDGE('',*,*,#3725,.F.);
#4727=ORIENTED_EDGE('',*,*,#3726,.F.);
#4728=ORIENTED_EDGE('',*,*,#3727,.T.);
#4729=ORIENTED_EDGE('',*,*,#3725,.T.);
#4730=ORIENTED_EDGE('',*,*,#3727,.F.);
#4731=ORIENTED_EDGE('',*,*,#3728,.F.);
#4732=ORIENTED_EDGE('',*,*,#3729,.T.);
#4733=ORIENTED_EDGE('',*,*,#3730,.T.);
#4734=ORIENTED_EDGE('',*,*,#3729,.F.);
#4735=ORIENTED_EDGE('',*,*,#3728,.T.);
#4736=ORIENTED_EDGE('',*,*,#3726,.T.);
#4737=ORIENTED_EDGE('',*,*,#3721,.T.);
#4738=ORIENTED_EDGE('',*,*,#3718,.T.);
#4739=ORIENTED_EDGE('',*,*,#3715,.T.);
#4740=ORIENTED_EDGE('',*,*,#3712,.T.);
#4741=ORIENTED_EDGE('',*,*,#3730,.F.);
#4742=ORIENTED_EDGE('',*,*,#3722,.T.);
#4743=ORIENTED_EDGE('',*,*,#3719,.T.);
#4744=ORIENTED_EDGE('',*,*,#3716,.T.);
#4745=ORIENTED_EDGE('',*,*,#3713,.T.);
#4746=ORIENTED_EDGE('',*,*,#3710,.T.);
#6022=CYLINDRICAL_SURFACE('',#7119,0.225);
#6023=CYLINDRICAL_SURFACE('',#7122,0.225);
#6024=CYLINDRICAL_SURFACE('',#7125,0.225);
#6025=CYLINDRICAL_SURFACE('',#7128,0.225);
#6026=CYLINDRICAL_SURFACE('',#7131,2.59);
#6027=CYLINDRICAL_SURFACE('',#7136,2.);
#6028=CYLINDRICAL_SURFACE('',#7138,4.);
#6178=ADVANCED_FACE('',(#953),#6022,.F.);
#6179=ADVANCED_FACE('',(#954),#6023,.F.);
#6180=ADVANCED_FACE('',(#955),#6024,.F.);
#6181=ADVANCED_FACE('',(#956),#6025,.F.);
#6182=ADVANCED_FACE('',(#957),#6026,.T.);
#6183=ADVANCED_FACE('',(#958,#572),#695,.F.);
#6184=ADVANCED_FACE('',(#959),#6027,.F.);
#6185=ADVANCED_FACE('',(#960),#6028,.T.);
#6186=ADVANCED_FACE('',(#961,#573,#574,#575,#576,#577),#696,.T.);
#6187=ADVANCED_FACE('',(#962,#578,#579,#580,#581,#582),#697,.F.);
#6499=CLOSED_SHELL('',(#6178,#6179,#6180,#6181,#6182,#6183,#6184,#6185,
#6186,#6187));
#7118=AXIS2_PLACEMENT_3D('',#10304,#8229,#8230);
#7119=AXIS2_PLACEMENT_3D('',#10305,#8231,#8232);
#7120=AXIS2_PLACEMENT_3D('',#10307,#8233,#8234);
#7121=AXIS2_PLACEMENT_3D('',#10310,#8236,#8237);
#7122=AXIS2_PLACEMENT_3D('',#10311,#8238,#8239);
#7123=AXIS2_PLACEMENT_3D('',#10313,#8240,#8241);
#7124=AXIS2_PLACEMENT_3D('',#10316,#8243,#8244);
#7125=AXIS2_PLACEMENT_3D('',#10317,#8245,#8246);
#7126=AXIS2_PLACEMENT_3D('',#10319,#8247,#8248);
#7127=AXIS2_PLACEMENT_3D('',#10322,#8250,#8251);
#7128=AXIS2_PLACEMENT_3D('',#10323,#8252,#8253);
#7129=AXIS2_PLACEMENT_3D('',#10325,#8254,#8255);
#7130=AXIS2_PLACEMENT_3D('',#10328,#8257,#8258);
#7131=AXIS2_PLACEMENT_3D('',#10329,#8259,#8260);
#7132=AXIS2_PLACEMENT_3D('',#10331,#8261,#8262);
#7133=AXIS2_PLACEMENT_3D('',#10334,#8264,#8265);
#7134=AXIS2_PLACEMENT_3D('',#10335,#8266,#8267);
#7135=AXIS2_PLACEMENT_3D('',#10337,#8268,#8269);
#7136=AXIS2_PLACEMENT_3D('',#10338,#8270,#8271);
#7137=AXIS2_PLACEMENT_3D('',#10340,#8272,#8273);
#7138=AXIS2_PLACEMENT_3D('',#10342,#8275,#8276);
#7139=AXIS2_PLACEMENT_3D('',#10344,#8277,#8278);
#7140=AXIS2_PLACEMENT_3D('',#10347,#8280,#8281);
#7141=AXIS2_PLACEMENT_3D('',#10348,#8282,#8283);
#7142=AXIS2_PLACEMENT_3D('',#10349,#8284,#8285);
#8229=DIRECTION('axis',(0.,0.,1.));
#8230=DIRECTION('refdir',(1.,0.,0.));
#8231=DIRECTION('center_axis',(0.,1.,0.));
#8232=DIRECTION('ref_axis',(1.,0.,0.));
#8233=DIRECTION('center_axis',(0.,1.,0.));
#8234=DIRECTION('ref_axis',(1.,0.,0.));
#8235=DIRECTION('',(0.,1.,0.));
#8236=DIRECTION('center_axis',(0.,-1.,0.));
#8237=DIRECTION('ref_axis',(1.,0.,0.));
#8238=DIRECTION('center_axis',(0.,1.,0.));
#8239=DIRECTION('ref_axis',(1.,0.,0.));
#8240=DIRECTION('center_axis',(0.,1.,0.));
#8241=DIRECTION('ref_axis',(1.,0.,0.));
#8242=DIRECTION('',(0.,1.,0.));
#8243=DIRECTION('center_axis',(0.,-1.,0.));
#8244=DIRECTION('ref_axis',(1.,0.,0.));
#8245=DIRECTION('center_axis',(0.,1.,0.));
#8246=DIRECTION('ref_axis',(1.,0.,0.));
#8247=DIRECTION('center_axis',(0.,1.,0.));
#8248=DIRECTION('ref_axis',(1.,0.,0.));
#8249=DIRECTION('',(0.,1.,0.));
#8250=DIRECTION('center_axis',(0.,-1.,0.));
#8251=DIRECTION('ref_axis',(1.,0.,0.));
#8252=DIRECTION('center_axis',(0.,1.,0.));
#8253=DIRECTION('ref_axis',(1.,0.,0.));
#8254=DIRECTION('center_axis',(0.,1.,0.));
#8255=DIRECTION('ref_axis',(1.,0.,0.));
#8256=DIRECTION('',(0.,1.,0.));
#8257=DIRECTION('center_axis',(0.,-1.,0.));
#8258=DIRECTION('ref_axis',(1.,0.,0.));
#8259=DIRECTION('center_axis',(0.,1.,0.));
#8260=DIRECTION('ref_axis',(1.,0.,0.));
#8261=DIRECTION('center_axis',(0.,1.,0.));
#8262=DIRECTION('ref_axis',(1.,0.,0.));
#8263=DIRECTION('',(0.,-1.,0.));
#8264=DIRECTION('center_axis',(0.,1.,0.));
#8265=DIRECTION('ref_axis',(1.,0.,0.));
#8266=DIRECTION('center_axis',(0.,1.,0.));
#8267=DIRECTION('ref_axis',(1.,0.,0.));
#8268=DIRECTION('center_axis',(0.,-1.,0.));
#8269=DIRECTION('ref_axis',(1.,0.,0.));
#8270=DIRECTION('center_axis',(0.,1.,0.));
#8271=DIRECTION('ref_axis',(1.,0.,0.));
#8272=DIRECTION('center_axis',(0.,-1.,0.));
#8273=DIRECTION('ref_axis',(1.,0.,0.));
#8274=DIRECTION('',(0.,-1.,0.));
#8275=DIRECTION('center_axis',(0.,1.,0.));
#8276=DIRECTION('ref_axis',(1.,0.,0.));
#8277=DIRECTION('center_axis',(0.,1.,0.));
#8278=DIRECTION('ref_axis',(1.,0.,0.));
#8279=DIRECTION('',(0.,-1.,0.));
#8280=DIRECTION('center_axis',(0.,1.,0.));
#8281=DIRECTION('ref_axis',(1.,0.,0.));
#8282=DIRECTION('center_axis',(0.,1.,0.));
#8283=DIRECTION('ref_axis',(1.,0.,0.));
#8284=DIRECTION('center_axis',(0.,1.,0.));
#8285=DIRECTION('ref_axis',(1.,0.,0.));
#10304=CARTESIAN_POINT('',(0.,0.,0.));
#10305=CARTESIAN_POINT('Origin',(-3.3,5.9,8.));
#10306=CARTESIAN_POINT('',(-3.525,6.,8.));
#10307=CARTESIAN_POINT('Origin',(-3.3,6.,8.));
#10308=CARTESIAN_POINT('',(-3.525,6.4,8.));
#10309=CARTESIAN_POINT('',(-3.525,5.9,8.));
#10310=CARTESIAN_POINT('Origin',(-3.3,6.4,8.));
#10311=CARTESIAN_POINT('Origin',(2.02066721859313E-16,5.9,11.3));
#10312=CARTESIAN_POINT('',(-0.225,6.,11.3));
#10313=CARTESIAN_POINT('Origin',(2.02066721859313E-16,6.,11.3));
#10314=CARTESIAN_POINT('',(-0.225,6.4,11.3));
#10315=CARTESIAN_POINT('',(-0.225,5.9,11.3));
#10316=CARTESIAN_POINT('Origin',(2.02066721859313E-16,6.4,11.3));
#10317=CARTESIAN_POINT('Origin',(3.3,5.9,8.));
#10318=CARTESIAN_POINT('',(3.075,6.,8.));
#10319=CARTESIAN_POINT('Origin',(3.3,6.,8.));
#10320=CARTESIAN_POINT('',(3.075,6.4,8.));
#10321=CARTESIAN_POINT('',(3.075,5.9,8.));
#10322=CARTESIAN_POINT('Origin',(3.3,6.4,8.));
#10323=CARTESIAN_POINT('Origin',(-6.0620016557794E-16,5.9,4.7));
#10324=CARTESIAN_POINT('',(-0.225000000000001,6.,4.7));
#10325=CARTESIAN_POINT('Origin',(-6.0620016557794E-16,6.,4.7));
#10326=CARTESIAN_POINT('',(-0.225000000000001,6.4,4.7));
#10327=CARTESIAN_POINT('',(-0.225000000000001,5.9,4.7));
#10328=CARTESIAN_POINT('Origin',(-6.0620016557794E-16,6.4,4.7));
#10329=CARTESIAN_POINT('Origin',(0.,5.75,8.));
#10330=CARTESIAN_POINT('',(-2.59,6.,8.));
#10331=CARTESIAN_POINT('Origin',(0.,6.,8.));
#10332=CARTESIAN_POINT('',(-2.59,5.75,8.));
#10333=CARTESIAN_POINT('',(-2.59,5.75,8.));
#10334=CARTESIAN_POINT('Origin',(0.,5.75,8.));
#10335=CARTESIAN_POINT('Origin',(0.,5.75,8.));
#10336=CARTESIAN_POINT('',(-2.,5.75,8.));
#10337=CARTESIAN_POINT('Origin',(0.,5.75,8.));
#10338=CARTESIAN_POINT('Origin',(0.,6.,8.));
#10339=CARTESIAN_POINT('',(-2.,6.4,8.));
#10340=CARTESIAN_POINT('Origin',(0.,6.4,8.));
#10341=CARTESIAN_POINT('',(-2.,6.,8.));
#10342=CARTESIAN_POINT('Origin',(0.,6.,8.));
#10343=CARTESIAN_POINT('',(-4.,6.4,8.));
#10344=CARTESIAN_POINT('Origin',(0.,6.4,8.));
#10345=CARTESIAN_POINT('',(-4.,6.,8.));
#10346=CARTESIAN_POINT('',(-4.,6.,8.));
#10347=CARTESIAN_POINT('Origin',(0.,6.,8.));
#10348=CARTESIAN_POINT('Origin',(0.,6.4,8.));
#10349=CARTESIAN_POINT('Origin',(0.,6.,8.));
#12702=UNCERTAINTY_MEASURE_WITH_UNIT(LENGTH_MEASURE(0.001),#12784,
'DISTANCE_ACCURACY_VALUE',
'Maximum model space distance between geometric entities at asserted c
onnectivities');
#12739=UNCERTAINTY_MEASURE_WITH_UNIT(LENGTH_MEASURE(0.001),#12784,
'DISTANCE_ACCURACY_VALUE',
'Maximum model space distance between geometric entities at asserted c
onnectivities');
#12746=(
GEOMETRIC_REPRESENTATION_CONTEXT(3)
GLOBAL_UNCERTAINTY_ASSIGNED_CONTEXT((#12702))
GLOBAL_UNIT_ASSIGNED_CONTEXT((#12784,#12786,#12787))
REPRESENTATION_CONTEXT('','3D')
);
#12783=(
GEOMETRIC_REPRESENTATION_CONTEXT(3)
GLOBAL_UNCERTAINTY_ASSIGNED_CONTEXT((#12739))
GLOBAL_UNIT_ASSIGNED_CONTEXT((#12784,#12786,#12787))
REPRESENTATION_CONTEXT('','3D')
);
#12784=(
LENGTH_UNIT()
NAMED_UNIT(*)
SI_UNIT(.CENTI.,.METRE.)
);
#12786=(
NAMED_UNIT(*)
PLANE_ANGLE_UNIT()
SI_UNIT($,.RADIAN.)
);
#12787=(
NAMED_UNIT(*)
SI_UNIT($,.STERADIAN.)
SOLID_ANGLE_UNIT()
);
#12794=SHAPE_DEFINITION_REPRESENTATION(#12837,#12937);
#12837=PRODUCT_DEFINITION_SHAPE('',$,#12981);
#12937=SHAPE_REPRESENTATION('',(#7118),#12746);
#12974=PRODUCT_DEFINITION_CONTEXT('part definition',#13105,'design');
#12981=PRODUCT_DEFINITION('Bearing cap (1)','Bearing cap (1)',#13024,#12974);
#13024=PRODUCT_DEFINITION_FORMATION('',$,#13113);
#13105=APPLICATION_CONTEXT(
'Core Data for Automotive Mechanical Design Process');
#13106=PRODUCT_CONTEXT('part definition',#13105,'mechanical');
#13113=PRODUCT('Bearing cap (1)','Bearing cap (1)','Bearing cap (1)',(#13106));
#13206=COLOUR_RGB('Grey',0.48,0.52,0.57);
#13207=FILL_AREA_STYLE_COLOUR('',#13206);
#13208=FILL_AREA_STYLE('',(#13207));
#13209=SURFACE_STYLE_FILL_AREA(#13208);
#13210=SURFACE_SIDE_STYLE('',(#13209));
#13211=SURFACE_STYLE_USAGE(.BOTH.,#13210);
#13212=PRESENTATION_STYLE_ASSIGNMENT((#13211));
ENDSEC;
END-ISO-10303-21;
